ISO-10303-21;
HEADER;
/* Generated by software containing ST-Developer
 * from STEP Tools, Inc. (www.steptools.com) 
 */

FILE_DESCRIPTION(
/* description */ ('Worm-less right-angle friction wheel drive'),
/* implementation_level */ '2;1');

FILE_NAME(
/* name */ 'Bearing cap (4).step',
/* time_stamp */ '2026-10-28T03:22:36-07:00',
/* author */ (''),
/* organization */ (''),
/* preprocessor_version */ 'ST-DEVELOPER v20.2',
/* originating_system */ 'Autodesk Translation Framework v15.17.0.0',
/* authorisation */ '');

FILE_SCHEMA (('AUTOMOTIVE_DESIGN { 1 0 10303 214 3 1 1 }'));
ENDSEC;

DATA;
#10=MECHANICAL_DESIGN_GEOMETRIC_PRESENTATION_REPRESENTATION('',(#622),#17046);
#528=SHAPE_REPRESENTATION_RELATIONSHIP('SRR','None',#17271,#575);
#575=ADVANCED_BREP_SHAPE_REPRESENTATION('',(#676),#17007);
#622=STYLED_ITEM('',(#17591),#676);
#676=MANIFOLD_SOLID_BREP('Body1',#8177);
#837=FACE_BOUND('',#1947,.T.);
#838=FACE_BOUND('',#1951,.T.);
#839=FACE_BOUND('',#1952,.T.);
#840=FACE_BOUND('',#1953,.T.);
#841=FACE_BOUND('',#1954,.T.);
#842=FACE_BOUND('',#1955,.T.);
#843=FACE_BOUND('',#1957,.T.);
#844=FACE_BOUND('',#1958,.T.);
#845=FACE_BOUND('',#1959,.T.);
#846=FACE_BOUND('',#1960,.T.);
#847=FACE_BOUND('',#1961,.T.);
#1026=PLANE('',#9058);
#1027=PLANE('',#9065);
#1028=PLANE('',#9066);
#1353=FACE_OUTER_BOUND('',#1941,.T.);
#1354=FACE_OUTER_BOUND('',#1942,.T.);
#1355=FACE_OUTER_BOUND('',#1943,.T.);
#1356=FACE_OUTER_BOUND('',#1944,.T.);
#1357=FACE_OUTER_BOUND('',#1945,.T.);
#1358=FACE_OUTER_BOUND('',#1946,.T.);
#1359=FACE_OUTER_BOUND('',#1948,.T.);
#1360=FACE_OUTER_BOUND('',#1949,.T.);
#1361=FACE_OUTER_BOUND('',#1950,.T.);
#1362=FACE_OUTER_BOUND('',#1956,.T.);
#1941=EDGE_LOOP('',(#6248,#6249,#6250,#6251));
#1942=EDGE_LOOP('',(#6252,#6253,#6254,#6255));
#1943=EDGE_LOOP('',(#6256,#6257,#6258,#6259));
#1944=EDGE_LOOP('',(#6260,#6261,#6262,#6263));
#1945=EDGE_LOOP('',(#6264,#6265,#6266,#6267));
#1946=EDGE_LOOP('',(#6268));
#1947=EDGE_LOOP('',(#6269));
#1948=EDGE_LOOP('',(#6270,#6271,#6272,#6273));
#1949=EDGE_LOOP('',(#6274,#6275,#6276,#6277));
#1950=EDGE_LOOP('',(#6278));
#1951=EDGE_LOOP('',(#6279));
#1952=EDGE_LOOP('',(#6280));
#1953=EDGE_LOOP('',(#6281));
#1954=EDGE_LOOP('',(#6282));
#1955=EDGE_LOOP('',(#6283));
#1956=EDGE_LOOP('',(#6284));
#1957=EDGE_LOOP('',(#6285));
#1958=EDGE_LOOP('',(#6286));
#1959=EDGE_LOOP('',(#6287));
#1960=EDGE_LOOP('',(#6288));
#1961=EDGE_LOOP('',(#6289));
#2592=LINE('',#13133,#3132);
#2593=LINE('',#13139,#3133);
#2594=LINE('',#13145,#3134);
#2595=LINE('',#13151,#3135);
#2596=LINE('',#13157,#3136);
#2597=LINE('',#13164,#3137);
#2598=LINE('',#13170,#3138);
#3132=VECTOR('',#10594,0.225);
#3133=VECTOR('',#10601,0.225);
#3134=VECTOR('',#10608,0.225);
#3135=VECTOR('',#10615,0.225);
#3136=VECTOR('',#10622,1.59);
#3137=VECTOR('',#10631,1.2);
#3138=VECTOR('',#10638,2.4);
#3599=CIRCLE('',#9044,0.225);
#3600=CIRCLE('',#9045,0.225);
#3601=CIRCLE('',#9047,0.225);
#3602=CIRCLE('',#9048,0.225);
#3603=CIRCLE('',#9050,0.225);
#3604=CIRCLE('',#9051,0.225);
#3605=CIRCLE('',#9053,0.225);
#3606=CIRCLE('',#9054,0.225);
#3607=CIRCLE('',#9056,1.59);
#3608=CIRCLE('',#9057,1.59);
#3609=CIRCLE('',#9059,1.2);
#3610=CIRCLE('',#9061,1.2);
#3611=CIRCLE('',#9063,2.4);
#3612=CIRCLE('',#9064,2.4);
#4107=VERTEX_POINT('',#13130);
#4108=VERTEX_POINT('',#13132);
#4109=VERTEX_POINT('',#13136);
#4110=VERTEX_POINT('',#13138);
#4111=VERTEX_POINT('',#13142);
#4112=VERTEX_POINT('',#13144);
#4113=VERTEX_POINT('',#13148);
#4114=VERTEX_POINT('',#13150);
#4115=VERTEX_POINT('',#13154);
#4116=VERTEX_POINT('',#13156);
#4117=VERTEX_POINT('',#13160);
#4118=VERTEX_POINT('',#13163);
#4119=VERTEX_POINT('',#13167);
#4120=VERTEX_POINT('',#13169);
#4893=EDGE_CURVE('',#4107,#4107,#3599,.T.);
#4894=EDGE_CURVE('',#4107,#4108,#2592,.T.);
#4895=EDGE_CURVE('',#4108,#4108,#3600,.T.);
#4896=EDGE_CURVE('',#4109,#4109,#3601,.T.);
#4897=EDGE_CURVE('',#4109,#4110,#2593,.T.);
#4898=EDGE_CURVE('',#4110,#4110,#3602,.T.);
#4899=EDGE_CURVE('',#4111,#4111,#3603,.T.);
#4900=EDGE_CURVE('',#4111,#4112,#2594,.T.);
#4901=EDGE_CURVE('',#4112,#4112,#3604,.T.);
#4902=EDGE_CURVE('',#4113,#4113,#3605,.T.);
#4903=EDGE_CURVE('',#4113,#4114,#2595,.T.);
#4904=EDGE_CURVE('',#4114,#4114,#3606,.T.);
#4905=EDGE_CURVE('',#4115,#4115,#3607,.T.);
#4906=EDGE_CURVE('',#4115,#4116,#2596,.T.);
#4907=EDGE_CURVE('',#4116,#4116,#3608,.T.);
#4908=EDGE_CURVE('',#4117,#4117,#3609,.T.);
#4909=EDGE_CURVE('',#4117,#4118,#2597,.T.);
#4910=EDGE_CURVE('',#4118,#4118,#3610,.T.);
#4911=EDGE_CURVE('',#4119,#4119,#3611,.T.);
#4912=EDGE_CURVE('',#4119,#4120,#2598,.T.);
#4913=EDGE_CURVE('',#4120,#4120,#3612,.T.);
#6248=ORIENTED_EDGE('',*,*,#4893,.F.);
#6249=ORIENTED_EDGE('',*,*,#4894,.T.);
#6250=ORIENTED_EDGE('',*,*,#4895,.F.);
#6251=ORIENTED_EDGE('',*,*,#4894,.F.);
#6252=ORIENTED_EDGE('',*,*,#4896,.F.);
#6253=ORIENTED_EDGE('',*,*,#4897,.T.);
#6254=ORIENTED_EDGE('',*,*,#4898,.F.);
#6255=ORIENTED_EDGE('',*,*,#4897,.F.);
#6256=ORIENTED_EDGE('',*,*,#4899,.F.);
#6257=ORIENTED_EDGE('',*,*,#4900,.T.);
#6258=ORIENTED_EDGE('',*,*,#4901,.F.);
#6259=ORIENTED_EDGE('',*,*,#4900,.F.);
#6260=ORIENTED_EDGE('',*,*,#4902,.F.);
#6261=ORIENTED_EDGE('',*,*,#4903,.T.);
#6262=ORIENTED_EDGE('',*,*,#4904,.F.);
#6263=ORIENTED_EDGE('',*,*,#4903,.F.);
#6264=ORIENTED_EDGE('',*,*,#4905,.F.);
#6265=ORIENTED_EDGE('',*,*,#4906,.T.);
#6266=ORIENTED_EDGE('',*,*,#4907,.F.);
#6267=ORIENTED_EDGE('',*,*,#4906,.F.);
#6268=ORIENTED_EDGE('',*,*,#4905,.T.);
#6269=ORIENTED_EDGE('',*,*,#4908,.T.);
#6270=ORIENTED_EDGE('',*,*,#4908,.F.);
#6271=ORIENTED_EDGE('',*,*,#4909,.T.);
#6272=ORIENTED_EDGE('',*,*,#4910,.T.);
#6273=ORIENTED_EDGE('',*,*,#4909,.F.);
#6274=ORIENTED_EDGE('',*,*,#4911,.F.);
#6275=ORIENTED_EDGE('',*,*,#4912,.T.);
#6276=ORIENTED_EDGE('',*,*,#4913,.T.);
#6277=ORIENTED_EDGE('',*,*,#4912,.F.);
#6278=ORIENTED_EDGE('',*,*,#4911,.T.);
#6279=ORIENTED_EDGE('',*,*,#4907,.T.);
#6280=ORIENTED_EDGE('',*,*,#4904,.T.);
#6281=ORIENTED_EDGE('',*,*,#4901,.T.);
#6282=ORIENTED_EDGE('',*,*,#4898,.T.);
#6283=ORIENTED_EDGE('',*,*,#4895,.T.);
#6284=ORIENTED_EDGE('',*,*,#4913,.F.);
#6285=ORIENTED_EDGE('',*,*,#4910,.F.);
#6286=ORIENTED_EDGE('',*,*,#4902,.T.);
#6287=ORIENTED_EDGE('',*,*,#4899,.T.);
#6288=ORIENTED_EDGE('',*,*,#4896,.T.);
#6289=ORIENTED_EDGE('',*,*,#4893,.T.);
#7601=CYLINDRICAL_SURFACE('',#9043,0.225);
#7602=CYLINDRICAL_SURFACE('',#9046,0.225);
#7603=CYLINDRICAL_SURFACE('',#9049,0.225);
#7604=CYLINDRICAL_SURFACE('',#9052,0.225);
#7605=CYLINDRICAL_SURFACE('',#9055,1.59);
#7606=CYLINDRICAL_SURFACE('',#9060,1.2);
#7607=CYLINDRICAL_SURFACE('',#9062,2.4);
#7845=ADVANCED_FACE('',(#1353),#7601,.F.);
#7846=ADVANCED_FACE('',(#1354),#7602,.F.);
#7847=ADVANCED_FACE('',(#1355),#7603,.F.);
#7848=ADVANCED_FACE('',(#1356),#7604,.F.);
#7849=ADVANCED_FACE('',(#1357),#7605,.T.);
#7850=ADVANCED_FACE('',(#1358,#837),#1026,.T.);
#7851=ADVANCED_FACE('',(#1359),#7606,.F.);
#7852=ADVANCED_FACE('',(#1360),#7607,.T.);
#7853=ADVANCED_FACE('',(#1361,#838,#839,#840,#841,#842),#1027,.T.);
#7854=ADVANCED_FACE('',(#1362,#843,#844,#845,#846,#847),#1028,.F.);
#8177=CLOSED_SHELL('',(#7845,#7846,#7847,#7848,#7849,#7850,#7851,#7852,
#7853,#7854));
#9042=AXIS2_PLACEMENT_3D('',#13128,#10588,#10589);
#9043=AXIS2_PLACEMENT_3D('',#13129,#10590,#10591);
#9044=AXIS2_PLACEMENT_3D('',#13131,#10592,#10593);
#9045=AXIS2_PLACEMENT_3D('',#13134,#10595,#10596);
#9046=AXIS2_PLACEMENT_3D('',#13135,#10597,#10598);
#9047=AXIS2_PLACEMENT_3D('',#13137,#10599,#10600);
#9048=AXIS2_PLACEMENT_3D('',#13140,#10602,#10603);
#9049=AXIS2_PLACEMENT_3D('',#13141,#10604,#10605);
#9050=AXIS2_PLACEMENT_3D('',#13143,#10606,#10607);
#9051=AXIS2_PLACEMENT_3D('',#13146,#10609,#10610);
#9052=AXIS2_PLACEMENT_3D('',#13147,#10611,#10612);
#9053=AXIS2_PLACEMENT_3D('',#13149,#10613,#10614);
#9054=AXIS2_PLACEMENT_3D('',#13152,#10616,#10617);
#9055=AXIS2_PLACEMENT_3D('',#13153,#10618,#10619);
#9056=AXIS2_PLACEMENT_3D('',#13155,#10620,#10621);
#9057=AXIS2_PLACEMENT_3D('',#13158,#10623,#10624);
#9058=AXIS2_PLACEMENT_3D('',#13159,#10625,#10626);
#9059=AXIS2_PLACEMENT_3D('',#13161,#10627,#10628);
#9060=AXIS2_PLACEMENT_3D('',#13162,#10629,#10630);
#9061=AXIS2_PLACEMENT_3D('',#13165,#10632,#10633);
#9062=AXIS2_PLACEMENT_3D('',#13166,#10634,#10635);
#9063=AXIS2_PLACEMENT_3D('',#13168,#10636,#10637);
#9064=AXIS2_PLACEMENT_3D('',#13171,#10639,#10640);
#9065=AXIS2_PLACEMENT_3D('',#13172,#10641,#10642);
#9066=AXIS2_PLACEMENT_3D('',#13173,#10643,#10644);
#10588=DIRECTION('axis',(0.,0.,1.));
#10589=DIRECTION('refdir',(1.,0.,0.));
#10590=DIRECTION('center_axis',(1.,0.,0.));
#10591=DIRECTION('ref_axis',(0.,0.,-1.));
#10592=DIRECTION('center_axis',(1.,0.,0.));
#10593=DIRECTION('ref_axis',(0.,0.,-1.));
#10594=DIRECTION('',(1.,0.,0.));
#10595=DIRECTION('center_axis',(-1.,0.,0.));
#10596=DIRECTION('ref_axis',(0.,0.,-1.));
#10597=DIRECTION('center_axis',(1.,0.,0.));
#10598=DIRECTION('ref_axis',(0.,0.,-1.));
#10599=DIRECTION('center_axis',(1.,0.,0.));
#10600=DIRECTION('ref_axis',(0.,0.,-1.));
#10601=DIRECTION('',(1.,0.,0.));
#10602=DIRECTION('center_axis',(-1.,0.,0.));
#10603=DIRECTION('ref_axis',(0.,0.,-1.));
#10604=DIRECTION('center_axis',(1.,0.,0.));
#10605=DIRECTION('ref_axis',(0.,0.,-1.));
#10606=DIRECTION('center_axis',(1.,0.,0.));
#10607=DIRECTION('ref_axis',(0.,0.,-1.));
#10608=DIRECTION('',(1.,0.,0.));
#10609=DIRECTION('center_axis',(-1.,0.,0.));
#10610=DIRECTION('ref_axis',(0.,0.,-1.));
#10611=DIRECTION('center_axis',(1.,0.,0.));
#10612=DIRECTION('ref_axis',(0.,0.,-1.));
#10613=DIRECTION('center_axis',(1.,0.,0.));
#10614=DIRECTION('ref_axis',(0.,0.,-1.));
#10615=DIRECTION('',(1.,0.,0.));
#10616=DIRECTION('center_axis',(-1.,0.,0.));
#10617=DIRECTION('ref_axis',(0.,0.,-1.));
#10618=DIRECTION('center_axis',(1.,0.,0.));
#10619=DIRECTION('ref_axis',(0.,0.,-1.));
#10620=DIRECTION('center_axis',(1.,0.,0.));
#10621=DIRECTION('ref_axis',(0.,0.,-1.));
#10622=DIRECTION('',(-1.,0.,0.));
#10623=DIRECTION('center_axis',(-1.,0.,0.));
#10624=DIRECTION('ref_axis',(0.,0.,-1.));
#10625=DIRECTION('center_axis',(1.,0.,0.));
#10626=DIRECTION('ref_axis',(0.,0.,-1.));
#10627=DIRECTION('center_axis',(-1.,0.,0.));
#10628=DIRECTION('ref_axis',(0.,0.,-1.));
#10629=DIRECTION('center_axis',(1.,0.,0.));
#10630=DIRECTION('ref_axis',(0.,0.,-1.));
#10631=DIRECTION('',(-1.,0.,0.));
#10632=DIRECTION('center_axis',(-1.,0.,0.));
#10633=DIRECTION('ref_axis',(0.,0.,-1.));
#10634=DIRECTION('center_axis',(1.,0.,0.));
#10635=DIRECTION('ref_axis',(0.,0.,-1.));
#10636=DIRECTION('center_axis',(1.,0.,0.));
#10637=DIRECTION('ref_axis',(0.,0.,-1.));
#10638=DIRECTION('',(-1.,0.,0.));
#10639=DIRECTION('center_axis',(1.,0.,0.));
#10640=DIRECTION('ref_axis',(0.,0.,-1.));
#10641=DIRECTION('center_axis',(1.,0.,0.));
#10642=DIRECTION('ref_axis',(0.,0.,-1.));
#10643=DIRECTION('center_axis',(1.,0.,0.));
#10644=DIRECTION('ref_axis',(0.,0.,-1.));
#13128=CARTESIAN_POINT('',(0.,0.,0.));
#13129=CARTESIAN_POINT('Origin',(-1.4,1.51507575950825,5.51507575950825));
#13130=CARTESIAN_POINT('',(-1.3,1.51507575950825,5.74007575950825));
#13131=CARTESIAN_POINT('Origin',(-1.3,1.51507575950825,5.51507575950825));
#13132=CARTESIAN_POINT('',(-1.1,1.51507575950825,5.74007575950825));
#13133=CARTESIAN_POINT('',(-1.4,1.51507575950825,5.74007575950825));
#13134=CARTESIAN_POINT('Origin',(-1.1,1.51507575950825,5.51507575950825));
#13135=CARTESIAN_POINT('Origin',(-1.4,1.51507575950825,8.48492424049175));
#13136=CARTESIAN_POINT('',(-1.3,1.51507575950825,8.70992424049175));
#13137=CARTESIAN_POINT('Origin',(-1.3,1.51507575950825,8.48492424049175));
#13138=CARTESIAN_POINT('',(-1.1,1.51507575950825,8.70992424049175));
#13139=CARTESIAN_POINT('',(-1.4,1.51507575950825,8.70992424049175));
#13140=CARTESIAN_POINT('Origin',(-1.1,1.51507575950825,8.48492424049175));
#13141=CARTESIAN_POINT('Origin',(-1.4,4.48492424049175,8.48492424049175));
#13142=CARTESIAN_POINT('',(-1.3,4.48492424049175,8.70992424049175));
#13143=CARTESIAN_POINT('Origin',(-1.3,4.48492424049175,8.48492424049175));
#13144=CARTESIAN_POINT('',(-1.1,4.48492424049175,8.70992424049175));
#13145=CARTESIAN_POINT('',(-1.4,4.48492424049175,8.70992424049175));
#13146=CARTESIAN_POINT('Origin',(-1.1,4.48492424049175,8.48492424049175));
#13147=CARTESIAN_POINT('Origin',(-1.4,4.48492424049175,5.51507575950825));
#13148=CARTESIAN_POINT('',(-1.3,4.48492424049175,5.74007575950825));
#13149=CARTESIAN_POINT('Origin',(-1.3,4.48492424049175,5.51507575950825));
#13150=CARTESIAN_POINT('',(-1.1,4.48492424049175,5.74007575950825));
#13151=CARTESIAN_POINT('',(-1.4,4.48492424049175,5.74007575950825));
#13152=CARTESIAN_POINT('Origin',(-1.1,4.48492424049175,5.51507575950825));
#13153=CARTESIAN_POINT('Origin',(-1.1,3.,7.));
#13154=CARTESIAN_POINT('',(-0.8,3.,8.59));
#13155=CARTESIAN_POINT('Origin',(-0.8,3.,7.));
#13156=CARTESIAN_POINT('',(-1.1,3.,8.59));
#13157=CARTESIAN_POINT('',(-1.1,3.,8.59));
#13158=CARTESIAN_POINT('Origin',(-1.1,3.,7.));
#13159=CARTESIAN_POINT('Origin',(-0.8,3.,7.));
#13160=CARTESIAN_POINT('',(-0.8,3.,8.2));
#13161=CARTESIAN_POINT('Origin',(-0.8,3.,7.));
#13162=CARTESIAN_POINT('Origin',(-1.3,3.,7.));
#13163=CARTESIAN_POINT('',(-1.3,3.,8.2));
#13164=CARTESIAN_POINT('',(-1.3,3.,8.2));
#13165=CARTESIAN_POINT('Origin',(-1.3,3.,7.));
#13166=CARTESIAN_POINT('Origin',(-1.3,3.,7.));
#13167=CARTESIAN_POINT('',(-1.1,3.,9.4));
#13168=CARTESIAN_POINT('Origin',(-1.1,3.,7.));
#13169=CARTESIAN_POINT('',(-1.3,3.,9.4));
#13170=CARTESIAN_POINT('',(-1.3,3.,9.4));
#13171=CARTESIAN_POINT('Origin',(-1.3,3.,7.));
#13172=CARTESIAN_POINT('Origin',(-1.1,3.,7.));
#13173=CARTESIAN_POINT('Origin',(-1.3,3.,7.));
#16954=UNCERTAINTY_MEASURE_WITH_UNIT(LENGTH_MEASURE(0.001),#17047,
'DISTANCE_ACCURACY_VALUE',
'Maximum model space distance between geometric entities at asserted c
onnectivities');
#16993=UNCERTAINTY_MEASURE_WITH_UNIT(LENGTH_MEASURE(0.001),#17047,
'DISTANCE_ACCURACY_VALUE',
'Maximum model space distance between geometric entities at asserted c
onnectivities');
#17007=(
GEOMETRIC_REPRESENTATION_CONTEXT(3)
GLOBAL_UNCERTAINTY_ASSIGNED_CONTEXT((#16954))
GLOBAL_UNIT_ASSIGNED_CONTEXT((#17047,#17049,#17050))
REPRESENTATION_CONTEXT('','3D')
);
#17046=(
GEOMETRIC_REPRESENTATION_CONTEXT(3)
GLOBAL_UNCERTAINTY_ASSIGNED_CONTEXT((#16993))
GLOBAL_UNIT_ASSIGNED_CONTEXT((#17047,#17049,#17050))
REPRESENTATION_CONTEXT('','3D')
);
#17047=(
LENGTH_UNIT()
NAMED_UNIT(*)
SI_UNIT(.CENTI.,.METRE.)
);
#17049=(
NAMED_UNIT(*)
PLANE_ANGLE_UNIT()
SI_UNIT($,.RADIAN.)
);
#17050=(
NAMED_UNIT(*)
SI_UNIT($,.STERADIAN.)
SOLID_ANGLE_UNIT()
);
#17064=SHAPE_DEFINITION_REPRESENTATION(#17116,#17271);
#17116=PRODUCT_DEFINITION_SHAPE('',$,#17324);
#17271=SHAPE_REPRESENTATION('',(#9042),#17007);
#17310=PRODUCT_DEFINITION_CONTEXT('part definition',#17468,'design');
#17324=PRODUCT_DEFINITION('Bearing cap (4)','Bearing cap (4)',#17376,#17310);
#17376=PRODUCT_DEFINITION_FORMATION('',$,#17483);
#17468=APPLICATION_CONTEXT(
'Core Data for Automotive Mechanical Design Process');
#17469=PRODUCT_CONTEXT('part definition',#17468,'mechanical');
#17483=PRODUCT('Bearing cap (4)','Bearing cap (4)','Bearing cap (4)',(#17469));
#17585=COLOUR_RGB('Grey',0.48,0.52,0.57);
#17586=FILL_AREA_STYLE_COLOUR('',#17585);
#17587=FILL_AREA_STYLE('',(#17586));
#17588=SURFACE_STYLE_FILL_AREA(#17587);
#17589=SURFACE_SIDE_STYLE('',(#17588));
#17590=SURFACE_STYLE_USAGE(.BOTH.,#17589);
#17591=PRESENTATION_STYLE_ASSIGNMENT((#17590));
ENDSEC;
END-ISO-10303-21;
